ISO-10303-21;
HEADER;
FILE_DESCRIPTION (('STEP AP214'),
    '1' );
FILE_NAME ('510 Pin Insulator.step',
    '2026-10-05T22:38:29',
    ( '' ),
    ( '' ),
    'SwSTEP 2.0',
    'SolidWorks 2020',
    '' );
FILE_SCHEMA (( 'AUTOMOTIVE_DESIGN' ));
ENDSEC;

DATA;
#4=VERTEX_POINT ( 'NONE', #45504 ) ;
#5=DIRECTION ( 'NONE',  ( 1.000000000000000000, 0.000000000000000000, 0.000000000000000000 ) ) ;
#17=FILL_AREA_STYLE_COLOUR ( '', #27665 ) ;
#67=CARTESIAN_POINT ( 'NONE',  ( 3.799999782336999754, 0.000000000000000000, -2.724999689663869962 ) ) ;
#77=AXIS2_PLACEMENT_3D ( 'NONE', #39446, #28974, #49587 ) ;
#104=EDGE_LOOP ( 'NONE', ( #11078, #29942, #13944, #17736 ) ) ;
#175=ORIENTED_EDGE ( 'NONE', *, *, #20604, .T. ) ;
#182=ORIENTED_EDGE ( 'NONE', *, *, #30805, .F. ) ;
#186=ADVANCED_FACE ( 'NONE', ( #41966 ), #57076, .T. ) ;
#305=APPLICATION_CONTEXT ( 'automotive_design' ) ;
#400=EDGE_LOOP ( 'NONE', ( #33240, #49205, #31738, #46802 ) ) ;
#476=DIRECTION ( 'NONE',  ( 1.000000000000000000, 0.000000000000000000, 0.000000000000000000 ) ) ;
#641=PLANE ( 'NONE',  #30391 ) ;
#676=CIRCLE ( 'NONE', #63137, 2.250000000000000000 ) ;
#681=VECTOR ( 'NONE', #12487, 1000.000000000000000 ) ;
#763=DIRECTION ( 'NONE',  ( -1.000000000000000000, 0.000000000000000000, 0.000000000000000000 ) ) ;
#785=ADVANCED_FACE ( 'NONE', ( #4383, #56855 ), #42154, .T. ) ;
#788=ORIENTED_EDGE ( 'NONE', *, *, #41401, .T. ) ;
#872=( LENGTH_UNIT ( ) NAMED_UNIT ( * ) SI_UNIT ( .MILLI., .METRE. ) );
#931=DIRECTION ( 'NONE',  ( -1.000000000000000000, 0.000000000000000000, 0.000000000000000000 ) ) ;
#1067=CARTESIAN_POINT ( 'NONE',  ( 4.574515983791000080E-07, 0.000000000000000000, 0.000000000000000000 ) ) ;
#1087=EDGE_LOOP ( 'NONE', ( #13122, #64415, #41237, #26351 ) ) ;
#1126=DIRECTION ( 'NONE',  ( -1.000000000000000000, 0.000000000000000000, 0.000000000000000000 ) ) ;
#1161=DIRECTION ( 'NONE',  ( 0.000000000000000000, -1.000000000000000000, 0.000000000000000000 ) ) ;
#1201=VERTEX_POINT ( 'NONE', #39231 ) ;
#1253=CARTESIAN_POINT ( 'NONE',  ( 1.850000260467999924, -1.625000260409000141, 4.909918417534999635E-10 ) ) ;
#1319=DIRECTION ( 'NONE',  ( 1.000000000000000000, 0.000000000000000000, 0.000000000000000000 ) ) ;
#1357=DIRECTION ( 'NONE',  ( -1.000000000000000000, 0.000000000000000000, 0.000000000000000000 ) ) ;
#1385=CONICAL_SURFACE ( 'NONE', #46000, 2.624999810206000372, 0.7853980665166908626 ) ;
#1874=CIRCLE ( 'NONE', #65486, 2.725000000000000089 ) ;
#1879=ADVANCED_FACE ( 'NONE', ( #43376 ), #33736, .F. ) ;
#1932=EDGE_CURVE ( 'NONE', #26882, #57519, #6915, .T. ) ;
#1994=FACE_OUTER_BOUND ( 'NONE', #41081, .T. ) ;
#2016=CARTESIAN_POINT ( 'NONE',  ( 0.1500001228197999914, -2.250000122783999856, 5.253497258719000289E-10 ) ) ;
#2076=ADVANCED_FACE ( 'NONE', ( #17491 ), #1385, .T. ) ;
#2165=ADVANCED_FACE ( 'NONE', ( #21860 ), #41558, .F. ) ;
#2178=CARTESIAN_POINT ( 'NONE',  ( 1.775000508673000077, 0.000000000000000000, -1.700000581162000035 ) ) ;
#2327=VECTOR ( 'NONE', #35567, 1000.000000000000114 ) ;
#2430=ORIENTED_EDGE ( 'NONE', *, *, #48721, .F. ) ;
#2523=ADVANCED_FACE ( 'NONE', ( #26872, #11808 ), #641, .F. ) ;
#2536=FACE_OUTER_BOUND ( 'NONE', #1087, .T. ) ;
#2583=FACE_OUTER_BOUND ( 'NONE', #6984, .T. ) ;
#2602=EDGE_CURVE ( 'NONE', #12398, #46125, #32801, .T. ) ;
#2603=ORIENTED_EDGE ( 'NONE', *, *, #7566, .T. ) ;
#2670=DIRECTION ( 'NONE',  ( 0.000000000000000000, -1.000000000000000000, 0.000000000000000000 ) ) ;
#2745=DIRECTION ( 'NONE',  ( -1.000000000000000000, 0.000000000000000000, 0.000000000000000000 ) ) ;
#2752=DIRECTION ( 'NONE',  ( -1.000000000000000000, 0.000000000000000000, 0.000000000000000000 ) ) ;
#3105=( GEOMETRIC_REPRESENTATION_CONTEXT ( 3 ) GLOBAL_UNCERTAINTY_ASSIGNED_CONTEXT ( ( #34387 ) ) GLOBAL_UNIT_ASSIGNED_CONTEXT ( ( #25560, #9466, #41637 ) ) REPRESENTATION_CONTEXT ( 'NONE', 'WORKASPACE' ) );
#3126=AXIS2_PLACEMENT_3D ( 'NONE', #24427, #2752, #45413 ) ;
#3280=ORIENTED_EDGE ( 'NONE', *, *, #41131, .T. ) ;
#3364=CYLINDRICAL_SURFACE ( 'NONE', #9751, 2.250000000000000000 ) ;
#3504=ORIENTED_EDGE ( 'NONE', *, *, #66051, .F. ) ;
#3546=EDGE_CURVE ( 'NONE', #37562, #19987, #34446, .T. ) ;
#3575=FACE_OUTER_BOUND ( 'NONE', #55151, .T. ) ;
#3603=ADVANCED_FACE ( 'NONE', ( #2536 ), #18284, .F. ) ;
#3723=LINE ( 'NONE', #41828, #11626 ) ;
#3731=CARTESIAN_POINT ( 'NONE',  ( 4.574515983791000080E-07, 0.000000000000000000, 0.000000000000000000 ) ) ;
#3762=ORIENTED_EDGE ( 'NONE', *, *, #58697, .T. ) ;
#3790=DIRECTION ( 'NONE',  ( 0.7071062208423759543, -0.7071073415302749909, 1.056388098201964040E-09 ) ) ;
#4006=DIRECTION ( 'NONE',  ( -1.000000000000000000, 0.000000000000000000, 0.000000000000000000 ) ) ;
#4163=EDGE_CURVE ( 'NONE', #63599, #49185, #68654, .T. ) ;
#4309=DIRECTION ( 'NONE',  ( -1.000000000000000000, 0.000000000000000000, 0.000000000000000000 ) ) ;
#4383=FACE_BOUND ( 'NONE', #9653, .T. ) ;
#4531=ORIENTED_EDGE ( 'NONE', *, *, #25878, .F. ) ;
#4546=DIRECTION ( 'NONE',  ( 0.000000000000000000, 0.000000000000000000, -1.000000000000000000 ) ) ;
#4730=CARTESIAN_POINT ( 'NONE',  ( 3.999999173945999686, 0.000000000000000000, 0.000000000000000000 ) ) ;
#4743=EDGE_CURVE ( 'NONE', #38406, #14135, #52593, .T. ) ;
#4911=SURFACE_STYLE_USAGE ( .BOTH. , #43709 ) ;
#4983=EDGE_LOOP ( 'NONE', ( #14221, #32056, #15892, #8250 ) ) ;
#5088=ORIENTED_EDGE ( 'NONE', *, *, #13195, .T. ) ;
#5439=VERTEX_POINT ( 'NONE', #16233 ) ;
#5594=EDGE_CURVE ( 'NONE', #47991, #50185, #52938, .T. ) ;
#5628=LINE ( 'NONE', #42016, #42879 ) ;
#5758=FILL_AREA_STYLE ('',( #6447 ) ) ;
#5939=AXIS2_PLACEMENT_3D ( 'NONE', #29957, #54164, #22352 ) ;
#6006=ORIENTED_EDGE ( 'NONE', *, *, #19479, .T. ) ;
#6038=CIRCLE ( 'NONE', #27262, 1.775000326287000219 ) ;
#6115=ORIENTED_EDGE ( 'NONE', *, *, #62966, .T. ) ;
#6182=ORIENTED_EDGE ( 'NONE', *, *, #19479, .F. ) ;
#6214=DIRECTION ( 'NONE',  ( 1.000000000000000000, -1.845552235241999991E-09, 8.866463766873999729E-13 ) ) ;
#6368=CARTESIAN_POINT ( 'NONE',  ( 3.800000448357999883, 0.000000000000000000, -1.625000000000000000 ) ) ;
#6392=CARTESIAN_POINT ( 'NONE',  ( 1.284778323729000017E-07, 0.000000000000000000, 0.000000000000000000 ) ) ;
#6441=VECTOR ( 'NONE', #36777, 1000.000000000000000 ) ;
#6447=FILL_AREA_STYLE_COLOUR ( '', #67940 ) ;
#6482=CARTESIAN_POINT ( 'NONE',  ( 0.07500030076246999577, 0.000000000000000000, 0.000000000000000000 ) ) ;
#6500=CIRCLE ( 'NONE', #23232, 2.250000000000000000 ) ;
#6520=ORIENTED_EDGE ( 'NONE', *, *, #50264, .T. ) ;
#6561=ORIENTED_EDGE ( 'NONE', *, *, #16171, .F. ) ;
#6652=ADVANCED_FACE ( 'NONE', ( #1994 ), #23316, .F. ) ;
#6860=DIRECTION ( 'NONE',  ( -1.000000000000000000, 0.000000000000000000, 0.000000000000000000 ) ) ;
#6915=CIRCLE ( 'NONE', #52735, 2.400000066501999818 ) ;
#6984=EDGE_LOOP ( 'NONE', ( #7840, #18310, #14962, #25943, #55344, #29450 ) ) ;
#7036=EDGE_CURVE ( 'NONE', #63565, #47991, #7324, .T. ) ;
#7172=ORIENTED_EDGE ( 'NONE', *, *, #5594, .T. ) ;
#7175=LINE ( 'NONE', #22555, #7702 ) ;
#7309=ORIENTED_EDGE ( 'NONE', *, *, #20604, .F. ) ;
#7324=LINE ( 'NONE', #28665, #26314 ) ;
#7566=EDGE_CURVE ( 'NONE', #12398, #45043, #59541, .T. ) ;
#7611=LINE ( 'NONE', #29992, #2327 ) ;
#7631=DIRECTION ( 'NONE',  ( 0.000000000000000000, -1.000000000000000000, 0.000000000000000000 ) ) ;
#7702=VECTOR ( 'NONE', #49826, 1000.000000000000114 ) ;
#7802=UNCERTAINTY_MEASURE_WITH_UNIT (LENGTH_MEASURE( 1.000000000000000082E-05 ), #48604, 'distance_accuracy_value', 'NONE');
#7832=DIRECTION ( 'NONE',  ( 0.000000000000000000, 1.000000000000000000, 0.000000000000000000 ) ) ;
#7840=ORIENTED_EDGE ( 'NONE', *, *, #60971, .T. ) ;
#7949=VECTOR ( 'NONE', #25673, 1000.000000000000114 ) ;
#7958=MANIFOLD_SOLID_BREP ( 'Stock-MAS-678-1', #44823 ) ;
#8004=FACE_BOUND ( 'NONE', #33386, .T. ) ;
#8147=ORIENTED_EDGE ( 'NONE', *, *, #62966, .F. ) ;
#8227=DIRECTION ( 'NONE',  ( 0.000000000000000000, -1.000000000000000000, 0.000000000000000000 ) ) ;
#8250=ORIENTED_EDGE ( 'NONE', *, *, #12146, .F. ) ;
#8303=EDGE_CURVE ( 'NONE', #42217, #12398, #34482, .T. ) ;
#8450=ADVANCED_FACE ( 'NONE', ( #40515 ), #27763, .F. ) ;
#8461=ORIENTED_EDGE ( 'NONE', *, *, #69132, .T. ) ;
#8931=EDGE_CURVE ( 'NONE', #63126, #1201, #64571, .T. ) ;
#9085=DIRECTION ( 'NONE',  ( 0.7071066261840305289, -0.7071069361890305327, 2.950983023348127876E-10 ) ) ;
#9115=ORIENTED_EDGE ( 'NONE', *, *, #4163, .F. ) ;
#9466=( NAMED_UNIT ( * ) PLANE_ANGLE_UNIT ( ) SI_UNIT ( $, .RADIAN. ) );
#9653=EDGE_LOOP ( 'NONE', ( #28500, #39028, #26519 ) ) ;
#9676=AXIS2_PLACEMENT_3D ( 'NONE', #40345, #19020, #18341 ) ;
#9751=AXIS2_PLACEMENT_3D ( 'NONE', #15238, #30985, #40771 ) ;
#10036=CARTESIAN_POINT ( 'NONE',  ( 0.1499996298882999846, 0.000000000000000000, -2.250000000000000000 ) ) ;
#10309=CARTESIAN_POINT ( 'NONE',  ( 3.999999615355000149, -1.825000384556999977, 7.326405409749999507E-10 ) ) ;
#10468=DIRECTION ( 'NONE',  ( 1.000000000000000000, 0.000000000000000000, 0.000000000000000000 ) ) ;
#10662=SURFACE_STYLE_FILL_AREA ( #5758 ) ;
#10772=FACE_OUTER_BOUND ( 'NONE', #62901, .T. ) ;
#10901=AXIS2_PLACEMENT_3D ( 'NONE', #60432, #50288, #27935 ) ;
#10998=ORIENTED_EDGE ( 'NONE', *, *, #53176, .F. ) ;
#11078=ORIENTED_EDGE ( 'NONE', *, *, #8931, .F. ) ;
#11372=VERTEX_POINT ( 'NONE', #44672 ) ;
#11453=CARTESIAN_POINT ( 'NONE',  ( 0.1500002361980000143, -2.725000000000000089, 0.000000000000000000 ) ) ;
#11581=FACE_OUTER_BOUND ( 'NONE', #26981, .T. ) ;
#11586=ORIENTED_EDGE ( 'NONE', *, *, #48527, .T. ) ;
#11626=VECTOR ( 'NONE', #52660, 1000.000000000000000 ) ;
#11808=FACE_OUTER_BOUND ( 'NONE', #34535, .T. ) ;
#11817=VERTEX_POINT ( 'NONE', #59612 ) ;
#12103=CARTESIAN_POINT ( 'NONE',  ( 3.999999173945999686, 1.825000327749000117, 0.000000000000000000 ) ) ;
#12146=EDGE_CURVE ( 'NONE', #14135, #47477, #34103, .T. ) ;
#12342=DIRECTION ( 'NONE',  ( -1.000000000000000000, 0.000000000000000000, 0.000000000000000000 ) ) ;
#12398=VERTEX_POINT ( 'NONE', #35725 ) ;
#12487=DIRECTION ( 'NONE',  ( 1.000000000000000000, 1.507841142982000116E-09, 1.100586469722000106E-11 ) ) ;
#12579=DIRECTION ( 'NONE',  ( 1.000000000000000000, 0.000000000000000000, 0.000000000000000000 ) ) ;
#12618=ADVANCED_FACE ( 'NONE', ( #8004, #29340 ), #50652, .T. ) ;
#12704=UNCERTAINTY_MEASURE_WITH_UNIT (LENGTH_MEASURE( 1.000000000000000082E-05 ), #872, 'distance_accuracy_value', 'NONE');
#12832=DIRECTION ( 'NONE',  ( -1.000000000000000000, 0.000000000000000000, 0.000000000000000000 ) ) ;
#12852=LINE ( 'NONE', #2016, #22731 ) ;
#13122=ORIENTED_EDGE ( 'NONE', *, *, #2602, .T. ) ;
#13150=MECHANICAL_DESIGN_GEOMETRIC_PRESENTATION_REPRESENTATION('',(#18731),#39947);
#13195=EDGE_CURVE ( 'NONE', #57519, #49507, #60784, .T. ) ;
#13373=ORIENTED_EDGE ( 'NONE', *, *, #42467, .F. ) ;
#13404=DIRECTION ( 'NONE',  ( 0.000000000000000000, 0.000000000000000000, -1.000000000000000000 ) ) ;
#13438=DIRECTION ( 'NONE',  ( -1.000000000000000000, 0.000000000000000000, 0.000000000000000000 ) ) ;
#13447=CARTESIAN_POINT ( 'NONE',  ( 3.999999855301999752, 0.000000000000000000, 0.000000000000000000 ) ) ;
#13705=AXIS2_PLACEMENT_3D ( 'NONE', #6482, #23263, #27473 ) ;
#13762=CIRCLE ( 'NONE', #52833, 1.625000000000000000 ) ;
#13797=VECTOR ( 'NONE', #59284, 1000.000000000000227 ) ;
#13832=ORIENTED_EDGE ( 'NONE', *, *, #52080, .F. ) ;
#13944=ORIENTED_EDGE ( 'NONE', *, *, #18793, .T. ) ;
#14094=AXIS2_PLACEMENT_3D ( 'NONE', #15472, #763, #48310 ) ;
#14100=ORIENTED_EDGE ( 'NONE', *, *, #46481, .T. ) ;
#14101=DIRECTION ( 'NONE',  ( 0.000000000000000000, 1.000000000000000000, 0.000000000000000000 ) ) ;
#14135=VERTEX_POINT ( 'NONE', #54944 ) ;
#14181=PRODUCT_CONTEXT ( 'NONE', #47174, 'mechanical' ) ;
#14221=ORIENTED_EDGE ( 'NONE', *, *, #4743, .F. ) ;
#14304=CARTESIAN_POINT ( 'NONE',  ( 0.07500022993665000914, 0.000000000000000000, 0.000000000000000000 ) ) ;
#14558=FACE_OUTER_BOUND ( 'NONE', #32501, .T. ) ;
#14731=CARTESIAN_POINT ( 'NONE',  ( 3.999999855301999752, -2.524999655449999825, 0.000000000000000000 ) ) ;
#14791=CONICAL_SURFACE ( 'NONE', #13705, 2.649999808707999893, 0.7853980705567794596 ) ;
#14917=CARTESIAN_POINT ( 'NONE',  ( 1.700000811628999964, 0.000000000000000000, 0.000000000000000000 ) ) ;
#14962=ORIENTED_EDGE ( 'NONE', *, *, #50264, .F. ) ;
#15103=VECTOR ( 'NONE', #27137, 1000.000000000000000 ) ;
#15145=ORIENTED_EDGE ( 'NONE', *, *, #64812, .T. ) ;
#15185=CARTESIAN_POINT ( 'NONE',  ( 0.1500001228197999914, 2.250000122783999856, -5.253495588359999773E-10 ) ) ;
#15217=ADVANCED_FACE ( 'NONE', ( #14558 ), #3364, .F. ) ;
#15238=CARTESIAN_POINT ( 'NONE',  ( 0.000000000000000000, 0.000000000000000000, 0.000000000000000000 ) ) ;
#15358=CARTESIAN_POINT ( 'NONE',  ( 3.799999782336999754, 0.000000000000000000, 0.000000000000000000 ) ) ;
#15472=CARTESIAN_POINT ( 'NONE',  ( 0.07500022993665000914, 0.000000000000000000, 0.000000000000000000 ) ) ;
#15504=CARTESIAN_POINT ( 'NONE',  ( 3.799999782336999754, 0.000000000000000000, 0.000000000000000000 ) ) ;
#15544=ORIENTED_EDGE ( 'NONE', *, *, #4163, .T. ) ;
#15665=EDGE_CURVE ( 'NONE', #11372, #57947, #68940, .T. ) ;
#15892=ORIENTED_EDGE ( 'NONE', *, *, #58391, .F. ) ;
#15907=SURFACE_SIDE_STYLE ('',( #10662 ) ) ;
#15964=CARTESIAN_POINT ( 'NONE',  ( 0.1500002361980000143, 0.000000000000000000, 0.000000000000000000 ) ) ;
#16014=DIRECTION ( 'NONE',  ( 0.000000000000000000, 1.000000000000000000, 0.000000000000000000 ) ) ;
#16171=EDGE_CURVE ( 'NONE', #19987, #63565, #56879, .T. ) ;
#16233=CARTESIAN_POINT ( 'NONE',  ( 4.574515983791000080E-07, 0.000000000000000000, -2.400000066502543827 ) ) ;
#16241=AXIS2_PLACEMENT_3D ( 'NONE', #57729, #19997, #30831 ) ;
#16382=ORIENTED_EDGE ( 'NONE', *, *, #25878, .T. ) ;
#16608=CARTESIAN_POINT ( 'NONE',  ( 1.284778341492999868E-07, 0.000000000000000000, -2.574999650349000024 ) ) ;
#16637=LINE ( 'NONE', #54042, #13797 ) ;
#16649=VERTEX_POINT ( 'NONE', #67 ) ;
#16701=ORIENTED_EDGE ( 'NONE', *, *, #69132, .F. ) ;
#16771=PRESENTATION_STYLE_ASSIGNMENT (( #4911 ) ) ;
#16854=EDGE_LOOP ( 'NONE', ( #16382, #3280, #10998, #5088 ) ) ;
#16975=LINE ( 'NONE', #1253, #15103 ) ;
#17049=DIRECTION ( 'NONE',  ( 0.000000000000000000, 1.000000000000000000, 0.000000000000000000 ) ) ;
#17213=LINE ( 'NONE', #38537, #30527 ) ;
#17272=CARTESIAN_POINT ( 'NONE',  ( 0.1500002361980000143, 0.000000000000000000, 0.000000000000000000 ) ) ;
#17317=ORIENTED_EDGE ( 'NONE', *, *, #3546, .T. ) ;
#17491=FACE_OUTER_BOUND ( 'NONE', #33972, .T. ) ;
#17736=ORIENTED_EDGE ( 'NONE', *, *, #22270, .F. ) ;
#17830=CARTESIAN_POINT ( 'NONE',  ( 1.849999551004999798, 0.000000000000000000, 0.000000000000000000 ) ) ;
#18189=AXIS2_PLACEMENT_3D ( 'NONE', #52059, #41580, #47866 ) ;
#18284=CYLINDRICAL_SURFACE ( 'NONE', #34967, 1.625000000000000000 ) ;
#18310=ORIENTED_EDGE ( 'NONE', *, *, #62037, .F. ) ;
#18341=DIRECTION ( 'NONE',  ( 1.000000000000000000, 0.000000000000000000, 0.000000000000000000 ) ) ;
#18689=CIRCLE ( 'NONE', #26520, 1.625000000000000000 ) ;
#18731=STYLED_ITEM ( 'NONE', ( #16771 ), #24370 ) ;
#18793=EDGE_CURVE ( 'NONE', #16649, #63146, #65949, .T. ) ;
#18835=ORIENTED_EDGE ( 'NONE', *, *, #15665, .F. ) ;
#19020=DIRECTION ( 'NONE',  ( 0.000000000000000000, 0.000000000000000000, 1.000000000000000000 ) ) ;
#19166=DIRECTION ( 'NONE',  ( 0.000000000000000000, 0.000000000000000000, -1.000000000000000000 ) ) ;
#19255=EDGE_CURVE ( 'NONE', #37562, #50185, #67804, .T. ) ;
#19348=VECTOR ( 'NONE', #50777, 1000.000000000000114 ) ;
#19479=EDGE_CURVE ( 'NONE', #63599, #63126, #40270, .T. ) ;
#19604=CIRCLE ( 'NONE', #37455, 1.625000000000000000 ) ;
#19646=CONICAL_SURFACE ( 'NONE', #28588, 2.649999808707999893, 0.7853980705567794596 ) ;
#19687=SHAPE_REPRESENTATION ( '510 Pin Insulator', ( #9676 ), #3105 ) ;
#19960=ORIENTED_EDGE ( 'NONE', *, *, #41131, .F. ) ;
#19987=VERTEX_POINT ( 'NONE', #39896 ) ;
#19997=DIRECTION ( 'NONE',  ( 1.000000000000000000, 0.000000000000000000, 0.000000000000000000 ) ) ;
#20060=ORIENTED_EDGE ( 'NONE', *, *, #64638, .F. ) ;
#20108=CARTESIAN_POINT ( 'NONE',  ( 1.849999551004999798, -1.625000000000000000, 0.000000000000000000 ) ) ;
#20237=DIRECTION ( 'NONE',  ( 1.000000000000000000, 0.000000000000000000, 0.000000000000000000 ) ) ;
#20343=AXIS2_PLACEMENT_3D ( 'NONE', #42510, #27123, #37943 ) ;
#20604=EDGE_CURVE ( 'NONE', #63146, #49185, #40256, .T. ) ;
#20625=ORIENTED_EDGE ( 'NONE', *, *, #65564, .F. ) ;
#20842=ORIENTED_EDGE ( 'NONE', *, *, #51796, .F. ) ;
#20917=AXIS2_PLACEMENT_3D ( 'NONE', #56043, #50806, #61979 ) ;
#21169=DIRECTION ( 'NONE',  ( -1.000000000000000000, 0.000000000000000000, 0.000000000000000000 ) ) ;
#21262=ADVANCED_FACE ( 'NONE', ( #10772 ), #38038, .F. ) ;
#21323=CARTESIAN_POINT ( 'NONE',  ( 3.899999681170999821, 0.000000000000000000, 0.000000000000000000 ) ) ;
#21327=DIRECTION ( 'NONE',  ( 0.000000000000000000, -1.000000000000000000, 0.000000000000000000 ) ) ;
#21577=CONICAL_SURFACE ( 'NONE', #39459, 1.700000581162000035, 0.7853984839373144844 ) ;
#21821=ORIENTED_EDGE ( 'NONE', *, *, #37013, .T. ) ;
#21860=FACE_OUTER_BOUND ( 'NONE', #43286, .T. ) ;
#22049=DIRECTION ( 'NONE',  ( -0.7071063294819032174, -0.7071072328909032700, 8.604668387600043697E-10 ) ) ;
#22186=( NAMED_UNIT ( * ) PLANE_ANGLE_UNIT ( ) SI_UNIT ( $, .RADIAN. ) );
#22270=EDGE_CURVE ( 'NONE', #1201, #63146, #7611, .T. ) ;
#22352=DIRECTION ( 'NONE',  ( 0.000000000000000000, 1.000000000000000000, 0.000000000000000000 ) ) ;
#22383=VECTOR ( 'NONE', #9085, 1000.000000000000000 ) ;
#22555=CARTESIAN_POINT ( 'NONE',  ( 1.746770393513999881E-07, 2.400000174626000238, -7.471637644860000521E-10 ) ) ;
#22600=CARTESIAN_POINT ( 'NONE',  ( 1.700000811628999964, -1.775000326287000219, 0.000000000000000000 ) ) ;
#22731=VECTOR ( 'NONE', #44332, 1000.000000000000114 ) ;
#22756=ORIENTED_EDGE ( 'NONE', *, *, #8931, .T. ) ;
#23089=LINE ( 'NONE', #43039, #33815 ) ;
#23232=AXIS2_PLACEMENT_3D ( 'NONE', #25615, #61989, #14101 ) ;
#23263=DIRECTION ( 'NONE',  ( 1.000000000000000000, 0.000000000000000000, 0.000000000000000000 ) ) ;
#23316=CYLINDRICAL_SURFACE ( 'NONE', #56458, 2.250000000000000000 ) ;
#23357=EDGE_CURVE ( 'NONE', #42217, #11817, #45859, .T. ) ;
#23506=CARTESIAN_POINT ( 'NONE',  ( 1.700000379347999857, -1.775000379263000028, 7.150861857908999773E-10 ) ) ;
#23632=ORIENTED_EDGE ( 'NONE', *, *, #4743, .T. ) ;
#23643=AXIS2_PLACEMENT_3D ( 'NONE', #62088, #52288, #63455 ) ;
#23895=VECTOR ( 'NONE', #62731, 1000.000000000000000 ) ;
#24055=CARTESIAN_POINT ( 'NONE',  ( 0.000000000000000000, 0.000000000000000000, 0.000000000000000000 ) ) ;
#24198=LINE ( 'NONE', #23506, #19348 ) ;
#24320=AXIS2_PLACEMENT_3D ( 'NONE', #51553, #57142, #68308 ) ;
#24370=ADVANCED_BREP_SHAPE_REPRESENTATION ( '', ( #7958, #9676 ), #3105 ) ;
#24426=CARTESIAN_POINT ( 'NONE',  ( 3.799999782336999754, 0.000000000000000000, 0.000000000000000000 ) ) ;
#24427=CARTESIAN_POINT ( 'NONE',  ( 1.699999999999999956, 0.000000000000000000, 0.000000000000000000 ) ) ;
#24687=DIRECTION ( 'NONE',  ( 1.000000000000000000, 0.000000000000000000, 0.000000000000000000 ) ) ;
#24915=PRODUCT_DEFINITION_SHAPE ( 'NONE', 'NONE',  #50496 ) ;
#25008=SHAPE_DEFINITION_REPRESENTATION ( #24915, #19687 ) ;
#25329=DIRECTION ( 'NONE',  ( 0.000000000000000000, 0.000000000000000000, -1.000000000000000000 ) ) ;
#25535=MECHANICAL_DESIGN_GEOMETRIC_PRESENTATION_REPRESENTATION('',(#50090),#63444);
#25560=( LENGTH_UNIT ( ) NAMED_UNIT ( * ) SI_UNIT ( .MILLI., .METRE. ) );
#25614=ADVANCED_FACE ( 'NONE', ( #46934 ), #31008, .T. ) ;
#25615=CARTESIAN_POINT ( 'NONE',  ( 1.699999999999999956, 0.000000000000000000, 0.000000000000000000 ) ) ;
#25673=DIRECTION ( 'NONE',  ( -0.7071066712931889375, -0.7071068910798888885, 1.670512803213974822E-10 ) ) ;
#25759=DIRECTION ( 'NONE',  ( 0.000000000000000000, -1.000000000000000000, 0.000000000000000000 ) ) ;
#25824=VECTOR ( 'NONE', #67168, 1000.000000000000227 ) ;
#25833=DIRECTION ( 'NONE',  ( 1.000000000000000000, 0.000000000000000000, 0.000000000000000000 ) ) ;
#25843=DIRECTION ( 'NONE',  ( 0.000000000000000000, -1.000000000000000000, 0.000000000000000000 ) ) ;
#25878=EDGE_CURVE ( 'NONE', #49507, #45933, #42131, .T. ) ;
#25917=CIRCLE ( 'NONE', #54915, 2.725000000000000089 ) ;
#25943=ORIENTED_EDGE ( 'NONE', *, *, #2602, .F. ) ;
#26136=CIRCLE ( 'NONE', #65195, 2.574999650349000024 ) ;
#26286=CIRCLE ( 'NONE', #66454, 1.825000327749000117 ) ;
#26314=VECTOR ( 'NONE', #37759, 1000.000000000000000 ) ;
#26351=ORIENTED_EDGE ( 'NONE', *, *, #7566, .F. ) ;
#26519=ORIENTED_EDGE ( 'NONE', *, *, #12146, .T. ) ;
#26520=AXIS2_PLACEMENT_3D ( 'NONE', #42935, #54108, #16014 ) ;
#26558=ORIENTED_EDGE ( 'NONE', *, *, #54484, .T. ) ;
#26872=FACE_BOUND ( 'NONE', #64442, .T. ) ;
#26882=VERTEX_POINT ( 'NONE', #63872 ) ;
#26981=EDGE_LOOP ( 'NONE', ( #26558, #11586, #64620, #44561 ) ) ;
#27100=PRESENTATION_STYLE_ASSIGNMENT (( #59243 ) ) ;
#27123=DIRECTION ( 'NONE',  ( -1.000000000000000000, 0.000000000000000000, 0.000000000000000000 ) ) ;
#27137=DIRECTION ( 'NONE',  ( 1.000000000000000000, 1.845552576849000024E-09, -8.865321528282000745E-13 ) ) ;
#27191=CARTESIAN_POINT ( 'NONE',  ( 0.1500001264883999708, -2.724999873498000103, -2.408237085193000045E-10 ) ) ;
#27262=AXIS2_PLACEMENT_3D ( 'NONE', #14917, #30319, #36239 ) ;
#27281=ORIENTED_EDGE ( 'NONE', *, *, #37013, .F. ) ;
#27322=ADVANCED_FACE ( 'NONE', ( #66641 ), #30286, .T. ) ;
#27366=DIRECTION ( 'NONE',  ( 0.000000000000000000, -1.000000000000000000, 0.000000000000000000 ) ) ;
#27424=CONICAL_SURFACE ( 'NONE', #60965, 1.725000594299999968, 0.7853984795078434722 ) ;
#27473=DIRECTION ( 'NONE',  ( 0.000000000000000000, 0.000000000000000000, -1.000000000000000000 ) ) ;
#27629=SURFACE_STYLE_FILL_AREA ( #42338 ) ;
#27651=ORIENTED_EDGE ( 'NONE', *, *, #37832, .F. ) ;
#27665=COLOUR_RGB ( '', 0.40784314, 0.44705882, 0.49803922) ;
#27763=CONICAL_SURFACE ( 'NONE', #61250, 2.325000277643999969, 0.7853982725543797727 ) ;
#27797=( NAMED_UNIT ( * ) SI_UNIT ( $, .STERADIAN. ) SOLID_ANGLE_UNIT ( ) );
#27935=DIRECTION ( 'NONE',  ( 0.000000000000000000, 1.000000000000000000, 0.000000000000000000 ) ) ;
#28016=CARTESIAN_POINT ( 'NONE',  ( 3.799999782336999754, -2.725000000000000089, 0.000000000000000000 ) ) ;
#28196=CARTESIAN_POINT ( 'NONE',  ( 3.800000448357999883, 0.000000000000000000, 0.000000000000000000 ) ) ;
#28262=CIRCLE ( 'NONE', #18189, 1.625000000000000000 ) ;
#28500=ORIENTED_EDGE ( 'NONE', *, *, #60579, .T. ) ;
#28588=AXIS2_PLACEMENT_3D ( 'NONE', #56038, #61289, #13404 ) ;
#28595=DIRECTION ( 'NONE',  ( 0.000000000000000000, -1.000000000000000000, 0.000000000000000000 ) ) ;
#28665=CARTESIAN_POINT ( 'NONE',  ( 0.07500030076246999577, 0.000000000000000000, -2.649999808707999893 ) ) ;
#28680=CARTESIAN_POINT ( 'NONE',  ( 3.899999681170999821, 0.000000000000000000, 0.000000000000000000 ) ) ;
#28974=DIRECTION ( 'NONE',  ( 1.000000000000000000, 0.000000000000000000, 0.000000000000000000 ) ) ;
#29166=ORIENTED_EDGE ( 'NONE', *, *, #64812, .F. ) ;
#29316=DIRECTION ( 'NONE',  ( 1.000000000000000000, 0.000000000000000000, 0.000000000000000000 ) ) ;
#29340=FACE_OUTER_BOUND ( 'NONE', #58833, .T. ) ;
#29450=ORIENTED_EDGE ( 'NONE', *, *, #30235, .F. ) ;
#29590=DIRECTION ( 'NONE',  ( 0.000000000000000000, 0.000000000000000000, -1.000000000000000000 ) ) ;
#29669=CYLINDRICAL_SURFACE ( 'NONE', #48784, 2.725000000000000089 ) ;
#29733=AXIS2_PLACEMENT_3D ( 'NONE', #57296, #25833, #31094 ) ;
#29916=DIRECTION ( 'NONE',  ( 0.000000000000000000, 1.000000000000000000, 0.000000000000000000 ) ) ;
#29942=ORIENTED_EDGE ( 'NONE', *, *, #35140, .T. ) ;
#29957=CARTESIAN_POINT ( 'NONE',  ( 1.849999551004999798, 0.000000000000000000, 0.000000000000000000 ) ) ;
#29992=CARTESIAN_POINT ( 'NONE',  ( 3.999999836924999386, 2.524999836911000273, 2.479012191990000139E-10 ) ) ;
#30235=EDGE_CURVE ( 'NONE', #45043, #42217, #13762, .T. ) ;
#30286=CYLINDRICAL_SURFACE ( 'NONE', #36482, 2.725000000000000089 ) ;
#30319=DIRECTION ( 'NONE',  ( 1.000000000000000000, 0.000000000000000000, 0.000000000000000000 ) ) ;
#30391=AXIS2_PLACEMENT_3D ( 'NONE', #32458, #53775, #17049 ) ;
#30527=VECTOR ( 'NONE', #3790, 1000.000000000000114 ) ;
#30729=AXIS2_PLACEMENT_3D ( 'NONE', #40350, #4309, #51520 ) ;
#30805=EDGE_CURVE ( 'NONE', #11372, #12398, #17213, .T. ) ;
#30831=DIRECTION ( 'NONE',  ( 0.000000000000000000, -1.000000000000000000, 0.000000000000000000 ) ) ;
#30895=ADVANCED_FACE ( 'NONE', ( #44019 ), #21577, .F. ) ;
#30902=DIRECTION ( 'NONE',  ( -1.000000000000000000, 0.000000000000000000, 0.000000000000000000 ) ) ;
#30985=DIRECTION ( 'NONE',  ( -1.000000000000000000, 0.000000000000000000, 0.000000000000000000 ) ) ;
#31008=CONICAL_SURFACE ( 'NONE', #20917, 2.649999808707999893, 0.7853980705567794596 ) ;
#31094=DIRECTION ( 'NONE',  ( 0.000000000000000000, -1.000000000000000000, 0.000000000000000000 ) ) ;
#31150=DIRECTION ( 'NONE',  ( -1.000000000000000000, 0.000000000000000000, 0.000000000000000000 ) ) ;
#31245=CARTESIAN_POINT ( 'NONE',  ( 3.999999173945999686, 0.000000000000000000, 0.000000000000000000 ) ) ;
#31246=DIRECTION ( 'NONE',  ( 0.000000000000000000, 1.000000000000000000, 0.000000000000000000 ) ) ;
#31738=ORIENTED_EDGE ( 'NONE', *, *, #37062, .F. ) ;
#31842=( NAMED_UNIT ( * ) PLANE_ANGLE_UNIT ( ) SI_UNIT ( $, .RADIAN. ) );
#31852=CARTESIAN_POINT ( 'NONE',  ( 0.07500022993665000914, 0.000000000000000000, 0.000000000000000000 ) ) ;
#32056=ORIENTED_EDGE ( 'NONE', *, *, #62037, .T. ) ;
#32421=ORIENTED_EDGE ( 'NONE', *, *, #54484, .F. ) ;
#32438=LINE ( 'NONE', #27191, #681 ) ;
#32458=CARTESIAN_POINT ( 'NONE',  ( 0.000000000000000000, 0.000000000000000000, 0.000000000000000000 ) ) ;
#32501=EDGE_LOOP ( 'NONE', ( #51015, #46161, #2430, #3504, #4531 ) ) ;
#32537=DIRECTION ( 'NONE',  ( 0.000000000000000000, 0.000000000000000000, -1.000000000000000000 ) ) ;
#32684=ORIENTED_EDGE ( 'NONE', *, *, #52080, .T. ) ;
#32801=LINE ( 'NONE', #43985, #39319 ) ;
#32970=ADVANCED_FACE ( 'NONE', ( #45613 ), #45207, .F. ) ;
#33240=ORIENTED_EDGE ( 'NONE', *, *, #30235, .T. ) ;
#33386=EDGE_LOOP ( 'NONE', ( #68273, #47863, #66668 ) ) ;
#33723=DIRECTION ( 'NONE',  ( 0.000000000000000000, -1.000000000000000000, 0.000000000000000000 ) ) ;
#33736=CONICAL_SURFACE ( 'NONE', #37074, 2.325000277643999969, 0.7853982725543797727 ) ;
#33815=VECTOR ( 'NONE', #64343, 1000.000000000000114 ) ;
#33909=DIRECTION ( 'NONE',  ( 0.000000000000000000, -1.000000000000000000, 0.000000000000000000 ) ) ;
#33972=EDGE_LOOP ( 'NONE', ( #59247, #6182, #15544, #36879 ) ) ;
#34103=CIRCLE ( 'NONE', #41922, 1.825000327749000117 ) ;
#34158=DIRECTION ( 'NONE',  ( 0.000000000000000000, -1.000000000000000000, 0.000000000000000000 ) ) ;
#34214=FACE_OUTER_BOUND ( 'NONE', #53461, .T. ) ;
#34387=UNCERTAINTY_MEASURE_WITH_UNIT (LENGTH_MEASURE( 1.000000000000000082E-05 ), #25560, 'distance_accuracy_value', 'NONE');
#34446=CIRCLE ( 'NONE', #43367, 2.574999650349000024 ) ;
#34482=CIRCLE ( 'NONE', #46743, 1.625000000000000000 ) ;
#34488=CARTESIAN_POINT ( 'NONE',  ( 1.775000508673000077, 0.000000000000000000, 0.000000000000000000 ) ) ;
#34535=EDGE_LOOP ( 'NONE', ( #17317, #65692, #3762 ) ) ;
#34918=CARTESIAN_POINT ( 'NONE',  ( 1.775000508673000077, 0.000000000000000000, 0.000000000000000000 ) ) ;
#34919=ORIENTED_EDGE ( 'NONE', *, *, #51796, .T. ) ;
#34928=ORIENTED_EDGE ( 'NONE', *, *, #58697, .F. ) ;
#34967=AXIS2_PLACEMENT_3D ( 'NONE', #60239, #12342, #65467 ) ;
#35140=EDGE_CURVE ( 'NONE', #63126, #16649, #16637, .T. ) ;
#35152=CARTESIAN_POINT ( 'NONE',  ( 3.899999503719000060, 0.000000000000000000, 0.000000000000000000 ) ) ;
#35239=EDGE_CURVE ( 'NONE', #11817, #11372, #37242, .T. ) ;
#35537=ORIENTED_EDGE ( 'NONE', *, *, #19255, .F. ) ;
#35538=PRODUCT ( '510 Pin Insulator', '510 Pin Insulator', '', ( #14181 ) ) ;
#35567=DIRECTION ( 'NONE',  ( -0.7071066712931889375, 0.7071068910798888885, -1.670485323815974547E-10 ) ) ;
#35725=CARTESIAN_POINT ( 'NONE',  ( 1.849999551004999798, 1.625000000000000000, 0.000000000000000000 ) ) ;
#35802=CARTESIAN_POINT ( 'NONE',  ( 3.999999173945999686, 0.000000000000000000, 0.000000000000000000 ) ) ;
#35918=ORIENTED_EDGE ( 'NONE', *, *, #42467, .T. ) ;
#36141=DIRECTION ( 'NONE',  ( 1.000000000000000000, 0.000000000000000000, 0.000000000000000000 ) ) ;
#36239=DIRECTION ( 'NONE',  ( 0.000000000000000000, -1.000000000000000000, 0.000000000000000000 ) ) ;
#36316=CARTESIAN_POINT ( 'NONE',  ( 3.899999503719000060, 0.000000000000000000, 0.000000000000000000 ) ) ;
#36471=VERTEX_POINT ( 'NONE', #69073 ) ;
#36482=AXIS2_PLACEMENT_3D ( 'NONE', #62422, #24687, #2670 ) ;
#36609=CARTESIAN_POINT ( 'NONE',  ( 1.849999551004999798, 0.000000000000000000, -1.625000000000000000 ) ) ;
#36728=ORIENTED_EDGE ( 'NONE', *, *, #35239, .F. ) ;
#36777=DIRECTION ( 'NONE',  ( 0.7071066261840305289, 0.7071069361890305327, -2.950954976001128386E-10 ) ) ;
#36879=ORIENTED_EDGE ( 'NONE', *, *, #39533, .T. ) ;
#37013=EDGE_CURVE ( 'NONE', #4, #63146, #3723, .T. ) ;
#37062=EDGE_CURVE ( 'NONE', #57947, #11817, #6038, .T. ) ;
#37074=AXIS2_PLACEMENT_3D ( 'NONE', #31852, #37093, #32537 ) ;
#37093=DIRECTION ( 'NONE',  ( -1.000000000000000000, 0.000000000000000000, 0.000000000000000000 ) ) ;
#37157=EDGE_LOOP ( 'NONE', ( #19960, #64303, #32421, #57038 ) ) ;
#37216=CARTESIAN_POINT ( 'NONE',  ( 3.800000448357999883, 1.625000000000000000, 0.000000000000000000 ) ) ;
#37242=CIRCLE ( 'NONE', #41681, 1.775000326287000219 ) ;
#37389=DIRECTION ( 'NONE',  ( 0.000000000000000000, -1.000000000000000000, 0.000000000000000000 ) ) ;
#37455=AXIS2_PLACEMENT_3D ( 'NONE', #28196, #6860, #49510 ) ;
#37562=VERTEX_POINT ( 'NONE', #46659 ) ;
#37759=DIRECTION ( 'NONE',  ( 0.7071068468348109537, 0.000000000000000000, -0.7071067155382779745 ) ) ;
#37832=EDGE_CURVE ( 'NONE', #43973, #46125, #5628, .T. ) ;
#37846=ORIENTED_EDGE ( 'NONE', *, *, #62426, .T. ) ;
#37911=DIRECTION ( 'NONE',  ( -0.7071063294819032174, 0.7071072328909032700, -8.604691786090042874E-10 ) ) ;
#37943=DIRECTION ( 'NONE',  ( 0.000000000000000000, 0.000000000000000000, -1.000000000000000000 ) ) ;
#38038=CONICAL_SURFACE ( 'NONE', #68181, 1.725000594299999968, 0.7853984795078434722 ) ;
#38162=ORIENTED_EDGE ( 'NONE', *, *, #53176, .T. ) ;
#38173=CARTESIAN_POINT ( 'NONE',  ( 0.1500002361980000143, 0.000000000000000000, 0.000000000000000000 ) ) ;
#38181=AXIS2_PLACEMENT_3D ( 'NONE', #61319, #13438, #33723 ) ;
#38406=VERTEX_POINT ( 'NONE', #6368 ) ;
#38460=CONICAL_SURFACE ( 'NONE', #52931, 1.700000581162000035, 0.7853984839373144844 ) ;
#38537=CARTESIAN_POINT ( 'NONE',  ( 1.700000379347999857, 1.775000379263000028, -7.150855879635999901E-10 ) ) ;
#38693=CONICAL_SURFACE ( 'NONE', #14094, 2.325000277643999969, 0.7853982725543797727 ) ;
#38815=DIRECTION ( 'NONE',  ( 0.000000000000000000, 0.000000000000000000, -1.000000000000000000 ) ) ;
#38940=AXIS2_PLACEMENT_3D ( 'NONE', #45016, #1319, #28595 ) ;
#39028=ORIENTED_EDGE ( 'NONE', *, *, #63369, .T. ) ;
#39160=DIRECTION ( 'NONE',  ( -1.000000000000000000, 0.000000000000000000, 0.000000000000000000 ) ) ;
#39231=CARTESIAN_POINT ( 'NONE',  ( 3.999999855301999752, 2.524999655449999825, 0.000000000000000000 ) ) ;
#39300=CARTESIAN_POINT ( 'NONE',  ( 1.284778341492999868E-07, 0.000000000000000000, 0.000000000000000000 ) ) ;
#39319=VECTOR ( 'NONE', #6214, 1000.000000000000000 ) ;
#39446=CARTESIAN_POINT ( 'NONE',  ( 3.999999855301999752, 0.000000000000000000, 0.000000000000000000 ) ) ;
#39459=AXIS2_PLACEMENT_3D ( 'NONE', #34488, #1357, #29590 ) ;
#39469=EDGE_LOOP ( 'NONE', ( #46590, #50441, #182, #36728 ) ) ;
#39533=EDGE_CURVE ( 'NONE', #49185, #16649, #25917, .T. ) ;
#39750=CIRCLE ( 'NONE', #29733, 2.250000000000000000 ) ;
#39852=ADVANCED_FACE ( 'NONE', ( #2583 ), #66554, .F. ) ;
#39896=CARTESIAN_POINT ( 'NONE',  ( 1.284778341492999868E-07, 2.574999650349000024, 0.000000000000000000 ) ) ;
#39915=EDGE_LOOP ( 'NONE', ( #8461, #6006, #22756 ) ) ;
#39919=CARTESIAN_POINT ( 'NONE',  ( 3.999999173945999686, -1.825000327749000117, 0.000000000000000000 ) ) ;
#39947=( GEOMETRIC_REPRESENTATION_CONTEXT ( 3 ) GLOBAL_UNCERTAINTY_ASSIGNED_CONTEXT ( ( #7802 ) ) GLOBAL_UNIT_ASSIGNED_CONTEXT ( ( #48604, #31842, #63975 ) ) REPRESENTATION_CONTEXT ( 'NONE', 'WORKASPACE' ) );
#40256=CIRCLE ( 'NONE', #61455, 2.725000000000000089 ) ;
#40270=CIRCLE ( 'NONE', #77, 2.524999655449999825 ) ;
#40319=ORIENTED_EDGE ( 'NONE', *, *, #7036, .F. ) ;
#40345=CARTESIAN_POINT ( 'NONE',  ( 0.000000000000000000, 0.000000000000000000, 0.000000000000000000 ) ) ;
#40350=CARTESIAN_POINT ( 'NONE',  ( 3.899999681170999821, 0.000000000000000000, 0.000000000000000000 ) ) ;
#40363=AXIS2_PLACEMENT_3D ( 'NONE', #21323, #31150, #4546 ) ;
#40515=FACE_OUTER_BOUND ( 'NONE', #37157, .T. ) ;
#40668=ADVANCED_FACE ( 'NONE', ( #60322 ), #14791, .T. ) ;
#40771=DIRECTION ( 'NONE',  ( 0.000000000000000000, -1.000000000000000000, 0.000000000000000000 ) ) ;
#41081=EDGE_LOOP ( 'NONE', ( #52816, #20842, #20625, #50318 ) ) ;
#41131=EDGE_CURVE ( 'NONE', #45933, #5439, #23089, .T. ) ;
#41224=ORIENTED_EDGE ( 'NONE', *, *, #37832, .T. ) ;
#41237=ORIENTED_EDGE ( 'NONE', *, *, #60971, .F. ) ;
#41401=EDGE_CURVE ( 'NONE', #44536, #46125, #28262, .T. ) ;
#41416=CARTESIAN_POINT ( 'NONE',  ( 0.1499996298882999846, 0.000000000000000000, 0.000000000000000000 ) ) ;
#41558=CONICAL_SURFACE ( 'NONE', #20343, 1.700000581162000035, 0.7853984839373144844 ) ;
#41580=DIRECTION ( 'NONE',  ( -1.000000000000000000, 0.000000000000000000, 0.000000000000000000 ) ) ;
#41637=( NAMED_UNIT ( * ) SI_UNIT ( $, .STERADIAN. ) SOLID_ANGLE_UNIT ( ) );
#41681=AXIS2_PLACEMENT_3D ( 'NONE', #62637, #52152, #8227 ) ;
#41757=LINE ( 'NONE', #15185, #57558 ) ;
#41828=CARTESIAN_POINT ( 'NONE',  ( 0.1500001264883999708, 2.724999873498000103, 2.408241100083999765E-10 ) ) ;
#41922=AXIS2_PLACEMENT_3D ( 'NONE', #35802, #30902, #67597 ) ;
#41966=FACE_OUTER_BOUND ( 'NONE', #65854, .T. ) ;
#42016=CARTESIAN_POINT ( 'NONE',  ( 3.999999615355000149, 1.825000384556999977, -7.326396463183999951E-10 ) ) ;
#42113=CARTESIAN_POINT ( 'NONE',  ( 3.899999503719000060, 0.000000000000000000, -1.725000594299999968 ) ) ;
#42131=CIRCLE ( 'NONE', #68917, 2.250000000000000000 ) ;
#42145=ADVANCED_FACE ( 'NONE', ( #34214 ), #29669, .T. ) ;
#42154=PLANE ( 'NONE',  #23643 ) ;
#42217=VERTEX_POINT ( 'NONE', #36609 ) ;
#42338=FILL_AREA_STYLE ('',( #17 ) ) ;
#42467=EDGE_CURVE ( 'NONE', #4, #47991, #1874, .T. ) ;
#42510=CARTESIAN_POINT ( 'NONE',  ( 1.775000508673000077, 0.000000000000000000, 0.000000000000000000 ) ) ;
#42853=AXIS2_PLACEMENT_3D ( 'NONE', #38173, #1126, #43781 ) ;
#42879=VECTOR ( 'NONE', #22049, 1000.000000000000114 ) ;
#42902=VECTOR ( 'NONE', #37911, 1000.000000000000114 ) ;
#42935=CARTESIAN_POINT ( 'NONE',  ( 3.800000448357999883, 0.000000000000000000, 0.000000000000000000 ) ) ;
#43039=CARTESIAN_POINT ( 'NONE',  ( 0.07500022993665000914, 0.000000000000000000, -2.325000277643999969 ) ) ;
#43286=EDGE_LOOP ( 'NONE', ( #61308, #2603, #20060, #18835 ) ) ;
#43367=AXIS2_PLACEMENT_3D ( 'NONE', #6392, #55690, #1161 ) ;
#43376=FACE_OUTER_BOUND ( 'NONE', #16854, .T. ) ;
#43709=SURFACE_SIDE_STYLE ('',( #27629 ) ) ;
#43781=DIRECTION ( 'NONE',  ( 0.000000000000000000, -1.000000000000000000, 0.000000000000000000 ) ) ;
#43973=VERTEX_POINT ( 'NONE', #12103 ) ;
#43985=CARTESIAN_POINT ( 'NONE',  ( 1.850000260467999924, 1.625000260409000141, -4.909918316425000356E-10 ) ) ;
#44019=FACE_OUTER_BOUND ( 'NONE', #400, .T. ) ;
#44163=CIRCLE ( 'NONE', #16241, 2.400000066501999818 ) ;
#44332=DIRECTION ( 'NONE',  ( 0.9999999999999967804, 7.921521013571943306E-08, -3.389355116421979744E-10 ) ) ;
#44536=VERTEX_POINT ( 'NONE', #56394 ) ;
#44561=ORIENTED_EDGE ( 'NONE', *, *, #1932, .F. ) ;
#44672=CARTESIAN_POINT ( 'NONE',  ( 1.700000811628999964, 1.775000326287000219, 0.000000000000000000 ) ) ;
#44725=CARTESIAN_POINT ( 'NONE',  ( 4.574515983791000080E-07, -2.400000066501999818, 0.000000000000000000 ) ) ;
#44823=CLOSED_SHELL ( 'NONE', ( #1879, #30895, #21262, #60448, #40668, #32970, #27322, #25614, #48997, #42145, #186, #2076, #785, #48576, #39852, #3603, #2165, #57566, #12618, #15217, #6652, #67487, #8450, #2523 ) ) ;
#45016=CARTESIAN_POINT ( 'NONE',  ( 3.999999855301999752, 0.000000000000000000, 0.000000000000000000 ) ) ;
#45043=VERTEX_POINT ( 'NONE', #20108 ) ;
#45204=CARTESIAN_POINT ( 'NONE',  ( 0.1500002361980000143, 0.000000000000000000, -2.724999730217442906 ) ) ;
#45207=CONICAL_SURFACE ( 'NONE', #54118, 1.725000594299999968, 0.7853984795078434722 ) ;
#45307=ORIENTED_EDGE ( 'NONE', *, *, #60579, .F. ) ;
#45413=DIRECTION ( 'NONE',  ( 0.000000000000000000, 0.000000000000000000, 1.000000000000000000 ) ) ;
#45504=CARTESIAN_POINT ( 'NONE',  ( 0.1500002361980000143, 2.725000000000000089, 0.000000000000000000 ) ) ;
#45613=FACE_OUTER_BOUND ( 'NONE', #66322, .T. ) ;
#45643=DIRECTION ( 'NONE',  ( 1.000000000000000000, 0.000000000000000000, 0.000000000000000000 ) ) ;
#45750=DIRECTION ( 'NONE',  ( 0.000000000000000000, -1.000000000000000000, 0.000000000000000000 ) ) ;
#45804=ORIENTED_EDGE ( 'NONE', *, *, #1932, .T. ) ;
#45859=LINE ( 'NONE', #2178, #25824 ) ;
#45933=VERTEX_POINT ( 'NONE', #10036 ) ;
#46000=AXIS2_PLACEMENT_3D ( 'NONE', #28680, #39160, #38815 ) ;
#46021=CARTESIAN_POINT ( 'NONE',  ( 3.799999782336999754, 2.725000000000000089, 0.000000000000000000 ) ) ;
#46125=VERTEX_POINT ( 'NONE', #37216 ) ;
#46161=ORIENTED_EDGE ( 'NONE', *, *, #46481, .F. ) ;
#46458=DIRECTION ( 'NONE',  ( 0.000000000000000000, 0.000000000000000000, -1.000000000000000000 ) ) ;
#46481=EDGE_CURVE ( 'NONE', #36471, #65786, #6500, .T. ) ;
#46590=ORIENTED_EDGE ( 'NONE', *, *, #23357, .F. ) ;
#46634=FACE_OUTER_BOUND ( 'NONE', #104, .T. ) ;
#46659=CARTESIAN_POINT ( 'NONE',  ( 1.284778341492999868E-07, -2.574999650349000024, 0.000000000000000000 ) ) ;
#46743=AXIS2_PLACEMENT_3D ( 'NONE', #17830, #12579, #33909 ) ;
#46802=ORIENTED_EDGE ( 'NONE', *, *, #64638, .T. ) ;
#46841=CARTESIAN_POINT ( 'NONE',  ( 1.593676744644999875E-07, -2.574999840614999425, -3.034235117293000092E-10 ) ) ;
#46873=CARTESIAN_POINT ( 'NONE',  ( 1.849999551004999798, 0.000000000000000000, 0.000000000000000000 ) ) ;
#46934=FACE_OUTER_BOUND ( 'NONE', #56749, .T. ) ;
#47033=LINE ( 'NONE', #10309, #42902 ) ;
#47171=DIRECTION ( 'NONE',  ( 1.000000000000000000, 0.000000000000000000, 0.000000000000000000 ) ) ;
#47174=APPLICATION_CONTEXT ( 'automotive_design' ) ;
#47350=DIRECTION ( 'NONE',  ( 0.9999999999999967804, -7.921520927618944111E-08, 3.389354038770978966E-10 ) ) ;
#47477=VERTEX_POINT ( 'NONE', #39919 ) ;
#47589=DIRECTION ( 'NONE',  ( 1.000000000000000000, 0.000000000000000000, 0.000000000000000000 ) ) ;
#47863=ORIENTED_EDGE ( 'NONE', *, *, #37062, .T. ) ;
#47866=DIRECTION ( 'NONE',  ( 0.000000000000000000, -1.000000000000000000, 0.000000000000000000 ) ) ;
#47991=VERTEX_POINT ( 'NONE', #45204 ) ;
#48310=DIRECTION ( 'NONE',  ( 0.000000000000000000, 0.000000000000000000, -1.000000000000000000 ) ) ;
#48527=EDGE_CURVE ( 'NONE', #59889, #49507, #676, .T. ) ;
#48576=ADVANCED_FACE ( 'NONE', ( #56467 ), #27424, .F. ) ;
#48604=( LENGTH_UNIT ( ) NAMED_UNIT ( * ) SI_UNIT ( .MILLI., .METRE. ) );
#48721=EDGE_CURVE ( 'NONE', #59889, #36471, #41757, .T. ) ;
#48784=AXIS2_PLACEMENT_3D ( 'NONE', #24055, #29316, #7631 ) ;
#48970=AXIS2_PLACEMENT_3D ( 'NONE', #3731, #476, #25759 ) ;
#48997=ADVANCED_FACE ( 'NONE', ( #3575 ), #19646, .T. ) ;
#49185=VERTEX_POINT ( 'NONE', #28016 ) ;
#49205=ORIENTED_EDGE ( 'NONE', *, *, #23357, .T. ) ;
#49507=VERTEX_POINT ( 'NONE', #66440 ) ;
#49510=DIRECTION ( 'NONE',  ( 0.000000000000000000, 1.000000000000000000, 0.000000000000000000 ) ) ;
#49587=DIRECTION ( 'NONE',  ( 0.000000000000000000, -1.000000000000000000, 0.000000000000000000 ) ) ;
#49826=DIRECTION ( 'NONE',  ( 0.7071065367651552247, -0.7071070256078553218, 1.045642193243934103E-09 ) ) ;
#50090=STYLED_ITEM ( 'NONE', ( #27100 ), #7958 ) ;
#50185=VERTEX_POINT ( 'NONE', #11453 ) ;
#50264=EDGE_CURVE ( 'NONE', #46125, #38406, #18689, .T. ) ;
#50288=DIRECTION ( 'NONE',  ( 1.000000000000000000, 0.000000000000000000, 0.000000000000000000 ) ) ;
#50318=ORIENTED_EDGE ( 'NONE', *, *, #48527, .F. ) ;
#50441=ORIENTED_EDGE ( 'NONE', *, *, #8303, .T. ) ;
#50490=DIRECTION ( 'NONE',  ( 1.000000000000000000, 0.000000000000000000, 0.000000000000000000 ) ) ;
#50496=PRODUCT_DEFINITION ( 'UNKNOWN', '', #53015, #52068 ) ;
#50652=PLANE ( 'NONE',  #3126 ) ;
#50777=DIRECTION ( 'NONE',  ( 0.7071062208423759543, 0.7071073415302749909, -1.056390868722963888E-09 ) ) ;
#50806=DIRECTION ( 'NONE',  ( 1.000000000000000000, 0.000000000000000000, 0.000000000000000000 ) ) ;
#51015=ORIENTED_EDGE ( 'NONE', *, *, #65564, .T. ) ;
#51251=ORIENTED_EDGE ( 'NONE', *, *, #63369, .F. ) ;
#51520=DIRECTION ( 'NONE',  ( 0.000000000000000000, 0.000000000000000000, -1.000000000000000000 ) ) ;
#51553=CARTESIAN_POINT ( 'NONE',  ( 1.699999999999999956, 0.000000000000000000, 0.000000000000000000 ) ) ;
#51570=ORIENTED_EDGE ( 'NONE', *, *, #19255, .T. ) ;
#51796=EDGE_CURVE ( 'NONE', #65786, #36471, #58903, .T. ) ;
#51909=CARTESIAN_POINT ( 'NONE',  ( 1.284778341492999868E-07, 0.000000000000000000, 0.000000000000000000 ) ) ;
#51924=CONICAL_SURFACE ( 'NONE', #30729, 2.624999810206000372, 0.7853980665166908626 ) ;
#52042=DIRECTION ( 'NONE',  ( 0.000000000000000000, 0.000000000000000000, -1.000000000000000000 ) ) ;
#52059=CARTESIAN_POINT ( 'NONE',  ( 3.800000448357999883, 0.000000000000000000, 0.000000000000000000 ) ) ;
#52068=PRODUCT_DEFINITION_CONTEXT ( 'detailed design', #305, 'design' ) ;
#52080=EDGE_CURVE ( 'NONE', #19987, #4, #63675, .T. ) ;
#52152=DIRECTION ( 'NONE',  ( 1.000000000000000000, 0.000000000000000000, 0.000000000000000000 ) ) ;
#52288=DIRECTION ( 'NONE',  ( 1.000000000000000000, 0.000000000000000000, 0.000000000000000000 ) ) ;
#52552=DIRECTION ( 'NONE',  ( -1.000000000000000000, 0.000000000000000000, 0.000000000000000000 ) ) ;
#52593=LINE ( 'NONE', #42113, #23895 ) ;
#52660=DIRECTION ( 'NONE',  ( 1.000000000000000000, -1.507841021312999948E-09, -1.100585032007000091E-11 ) ) ;
#52735=AXIS2_PLACEMENT_3D ( 'NONE', #1067, #47589, #68894 ) ;
#52816=ORIENTED_EDGE ( 'NONE', *, *, #48721, .T. ) ;
#52833=AXIS2_PLACEMENT_3D ( 'NONE', #46873, #5, #21327 ) ;
#52895=ORIENTED_EDGE ( 'NONE', *, *, #3546, .F. ) ;
#52931=AXIS2_PLACEMENT_3D ( 'NONE', #34918, #2745, #19166 ) ;
#52938=CIRCLE ( 'NONE', #64159, 2.725000000000000089 ) ;
#53015=PRODUCT_DEFINITION_FORMATION_WITH_SPECIFIED_SOURCE ( 'ANY', '', #35538, .NOT_KNOWN. ) ;
#53176=EDGE_CURVE ( 'NONE', #57519, #5439, #56813, .T. ) ;
#53461=EDGE_LOOP ( 'NONE', ( #6115, #7309, #27281, #29166 ) ) ;
#53537=AXIS2_PLACEMENT_3D ( 'NONE', #51909, #4006, #57848 ) ;
#53775=DIRECTION ( 'NONE',  ( 1.000000000000000000, 0.000000000000000000, 0.000000000000000000 ) ) ;
#53916=CARTESIAN_POINT ( 'NONE',  ( 0.1499996298882999846, 2.250000000000000000, 0.000000000000000000 ) ) ;
#54042=CARTESIAN_POINT ( 'NONE',  ( 3.899999681170999821, 0.000000000000000000, -2.624999810206000372 ) ) ;
#54108=DIRECTION ( 'NONE',  ( -1.000000000000000000, 0.000000000000000000, 0.000000000000000000 ) ) ;
#54118=AXIS2_PLACEMENT_3D ( 'NONE', #66918, #36141, #57451 ) ;
#54164=DIRECTION ( 'NONE',  ( 1.000000000000000000, 0.000000000000000000, 0.000000000000000000 ) ) ;
#54268=AXIS2_PLACEMENT_3D ( 'NONE', #4730, #21169, #58228 ) ;
#54369=CARTESIAN_POINT ( 'NONE',  ( 1.699999999999999956, -2.250000000000000000, 0.000000000000000000 ) ) ;
#54484=EDGE_CURVE ( 'NONE', #26882, #59889, #7175, .T. ) ;
#54781=AXIS2_PLACEMENT_3D ( 'NONE', #15358, #47171, #25843 ) ;
#54915=AXIS2_PLACEMENT_3D ( 'NONE', #24426, #62161, #45750 ) ;
#54944=CARTESIAN_POINT ( 'NONE',  ( 3.999999173945999686, 0.000000000000000000, -1.825000327748890427 ) ) ;
#55151=EDGE_LOOP ( 'NONE', ( #51570, #15145, #13832, #52895 ) ) ;
#55344=ORIENTED_EDGE ( 'NONE', *, *, #8303, .F. ) ;
#55546=CARTESIAN_POINT ( 'NONE',  ( 1.746770412757999755E-07, -2.400000174626000238, 7.471644989856000012E-10 ) ) ;
#55690=DIRECTION ( 'NONE',  ( -1.000000000000000000, 0.000000000000000000, 0.000000000000000000 ) ) ;
#55745=DIRECTION ( 'NONE',  ( 0.000000000000000000, 1.000000000000000000, 0.000000000000000000 ) ) ;
#55895=FACE_OUTER_BOUND ( 'NONE', #39469, .T. ) ;
#56038=CARTESIAN_POINT ( 'NONE',  ( 0.07500030076246999577, 0.000000000000000000, 0.000000000000000000 ) ) ;
#56043=CARTESIAN_POINT ( 'NONE',  ( 0.07500030076246999577, 0.000000000000000000, 0.000000000000000000 ) ) ;
#56394=CARTESIAN_POINT ( 'NONE',  ( 3.800000448357999883, -1.625000000000000000, 0.000000000000000000 ) ) ;
#56458=AXIS2_PLACEMENT_3D ( 'NONE', #60715, #12832, #34158 ) ;
#56467=FACE_OUTER_BOUND ( 'NONE', #4983, .T. ) ;
#56749=EDGE_LOOP ( 'NONE', ( #40319, #6561, #32684, #35918 ) ) ;
#56813=CIRCLE ( 'NONE', #48970, 2.400000066501999818 ) ;
#56855=FACE_OUTER_BOUND ( 'NONE', #39915, .T. ) ;
#56879=CIRCLE ( 'NONE', #53537, 2.574999650349000024 ) ;
#57038=ORIENTED_EDGE ( 'NONE', *, *, #62426, .F. ) ;
#57076=CONICAL_SURFACE ( 'NONE', #40363, 2.624999810206000372, 0.7853980665166908626 ) ;
#57142=DIRECTION ( 'NONE',  ( -1.000000000000000000, 0.000000000000000000, 0.000000000000000000 ) ) ;
#57296=CARTESIAN_POINT ( 'NONE',  ( 0.1499996298882999846, 0.000000000000000000, 0.000000000000000000 ) ) ;
#57437=ORIENTED_EDGE ( 'NONE', *, *, #22270, .T. ) ;
#57451=DIRECTION ( 'NONE',  ( 0.000000000000000000, 0.000000000000000000, -1.000000000000000000 ) ) ;
#57519=VERTEX_POINT ( 'NONE', #44725 ) ;
#57558=VECTOR ( 'NONE', #47350, 1000.000000000000114 ) ;
#57566=ADVANCED_FACE ( 'NONE', ( #55895 ), #38460, .F. ) ;
#57729=CARTESIAN_POINT ( 'NONE',  ( 4.574515983791000080E-07, 0.000000000000000000, 0.000000000000000000 ) ) ;
#57848=DIRECTION ( 'NONE',  ( 0.000000000000000000, 1.000000000000000000, 0.000000000000000000 ) ) ;
#57947=VERTEX_POINT ( 'NONE', #22600 ) ;
#58228=DIRECTION ( 'NONE',  ( 0.000000000000000000, 1.000000000000000000, 0.000000000000000000 ) ) ;
#58391=EDGE_CURVE ( 'NONE', #47477, #44536, #47033, .T. ) ;
#58436=CARTESIAN_POINT ( 'NONE',  ( 1.593676743165000117E-07, 2.574999840614999425, 3.034233182443000263E-10 ) ) ;
#58697=EDGE_CURVE ( 'NONE', #63565, #37562, #26136, .T. ) ;
#58833=EDGE_LOOP ( 'NONE', ( #14100, #34919 ) ) ;
#58881=ORIENTED_EDGE ( 'NONE', *, *, #39533, .F. ) ;
#58903=CIRCLE ( 'NONE', #24320, 2.250000000000000000 ) ;
#58997=ORIENTED_EDGE ( 'NONE', *, *, #58391, .T. ) ;
#59059=CARTESIAN_POINT ( 'NONE',  ( 0.1499996298882999846, 0.000000000000000000, 0.000000000000000000 ) ) ;
#59243=SURFACE_STYLE_USAGE ( .BOTH. , #15907 ) ;
#59247=ORIENTED_EDGE ( 'NONE', *, *, #35140, .F. ) ;
#59284=DIRECTION ( 'NONE',  ( -0.7071068496915847712, 0.000000000000000000, -0.7071067126815037129 ) ) ;
#59510=ORIENTED_EDGE ( 'NONE', *, *, #5594, .F. ) ;
#59541=CIRCLE ( 'NONE', #5939, 1.625000000000000000 ) ;
#59573=DIRECTION ( 'NONE',  ( -1.000000000000000000, 0.000000000000000000, 0.000000000000000000 ) ) ;
#59612=CARTESIAN_POINT ( 'NONE',  ( 1.700000811628999964, 0.000000000000000000, -1.775000326286801045 ) ) ;
#59651=DIRECTION ( 'NONE',  ( 0.000000000000000000, 1.000000000000000000, 0.000000000000000000 ) ) ;
#59746=DIRECTION ( 'NONE',  ( 0.7071065367651552247, 0.7071070256078553218, -1.045644868292934240E-09 ) ) ;
#59889=VERTEX_POINT ( 'NONE', #53916 ) ;
#59946=CIRCLE ( 'NONE', #65476, 2.524999655449999825 ) ;
#60239=CARTESIAN_POINT ( 'NONE',  ( 1.699999999999999956, 0.000000000000000000, 0.000000000000000000 ) ) ;
#60322=FACE_OUTER_BOUND ( 'NONE', #60862, .T. ) ;
#60432=CARTESIAN_POINT ( 'NONE',  ( 1.700000811628999964, 0.000000000000000000, 0.000000000000000000 ) ) ;
#60448=ADVANCED_FACE ( 'NONE', ( #46634 ), #51924, .T. ) ;
#60579=EDGE_CURVE ( 'NONE', #47477, #43973, #26286, .T. ) ;
#60715=CARTESIAN_POINT ( 'NONE',  ( 0.000000000000000000, 0.000000000000000000, 0.000000000000000000 ) ) ;
#60784=LINE ( 'NONE', #55546, #61173 ) ;
#60862=EDGE_LOOP ( 'NONE', ( #34928, #68603, #7172, #35537 ) ) ;
#60965=AXIS2_PLACEMENT_3D ( 'NONE', #35152, #45643, #25329 ) ;
#60970=CIRCLE ( 'NONE', #54268, 1.825000327749000117 ) ;
#60971=EDGE_CURVE ( 'NONE', #45043, #44536, #16975, .T. ) ;
#61173=VECTOR ( 'NONE', #59746, 1000.000000000000114 ) ;
#61250=AXIS2_PLACEMENT_3D ( 'NONE', #14304, #62858, #46458 ) ;
#61289=DIRECTION ( 'NONE',  ( 1.000000000000000000, 0.000000000000000000, 0.000000000000000000 ) ) ;
#61308=ORIENTED_EDGE ( 'NONE', *, *, #30805, .T. ) ;
#61319=CARTESIAN_POINT ( 'NONE',  ( 1.699999999999999956, 0.000000000000000000, 0.000000000000000000 ) ) ;
#61368=DIRECTION ( 'NONE',  ( 1.000000000000000000, 0.000000000000000000, 0.000000000000000000 ) ) ;
#61455=AXIS2_PLACEMENT_3D ( 'NONE', #15504, #68625, #31246 ) ;
#61979=DIRECTION ( 'NONE',  ( 0.000000000000000000, 0.000000000000000000, -1.000000000000000000 ) ) ;
#61989=DIRECTION ( 'NONE',  ( -1.000000000000000000, 0.000000000000000000, 0.000000000000000000 ) ) ;
#62037=EDGE_CURVE ( 'NONE', #38406, #44536, #19604, .T. ) ;
#62088=CARTESIAN_POINT ( 'NONE',  ( 4.000000000000000000, 0.000000000000000000, 0.000000000000000000 ) ) ;
#62161=DIRECTION ( 'NONE',  ( 1.000000000000000000, 0.000000000000000000, 0.000000000000000000 ) ) ;
#62422=CARTESIAN_POINT ( 'NONE',  ( 0.000000000000000000, 0.000000000000000000, 0.000000000000000000 ) ) ;
#62426=EDGE_CURVE ( 'NONE', #5439, #26882, #44163, .T. ) ;
#62637=CARTESIAN_POINT ( 'NONE',  ( 1.700000811628999964, 0.000000000000000000, 0.000000000000000000 ) ) ;
#62731=DIRECTION ( 'NONE',  ( 0.7071065576627081350, 0.000000000000000000, -0.7071070047103161782 ) ) ;
#62858=DIRECTION ( 'NONE',  ( -1.000000000000000000, 0.000000000000000000, 0.000000000000000000 ) ) ;
#62901=EDGE_LOOP ( 'NONE', ( #6520, #23632, #51251, #41224 ) ) ;
#62966=EDGE_CURVE ( 'NONE', #50185, #49185, #32438, .T. ) ;
#63126=VERTEX_POINT ( 'NONE', #66218 ) ;
#63137=AXIS2_PLACEMENT_3D ( 'NONE', #41416, #61368, #29916 ) ;
#63146=VERTEX_POINT ( 'NONE', #46021 ) ;
#63369=EDGE_CURVE ( 'NONE', #43973, #14135, #60970, .T. ) ;
#63409=CARTESIAN_POINT ( 'NONE',  ( 3.999999836924999386, -2.524999836911000273, -2.479015424680000399E-10 ) ) ;
#63444=( GEOMETRIC_REPRESENTATION_CONTEXT ( 3 ) GLOBAL_UNCERTAINTY_ASSIGNED_CONTEXT ( ( #12704 ) ) GLOBAL_UNIT_ASSIGNED_CONTEXT ( ( #872, #22186, #27797 ) ) REPRESENTATION_CONTEXT ( 'NONE', 'WORKASPACE' ) );
#63455=DIRECTION ( 'NONE',  ( 0.000000000000000000, 1.000000000000000000, 0.000000000000000000 ) ) ;
#63565=VERTEX_POINT ( 'NONE', #16608 ) ;
#63599=VERTEX_POINT ( 'NONE', #14731 ) ;
#63638=EDGE_LOOP ( 'NONE', ( #21821, #66891, #58881, #8147, #59510, #13373 ) ) ;
#63675=LINE ( 'NONE', #58436, #6441 ) ;
#63872=CARTESIAN_POINT ( 'NONE',  ( 4.574515983791000080E-07, 2.400000066501999818, 0.000000000000000000 ) ) ;
#63975=( NAMED_UNIT ( * ) SI_UNIT ( $, .STERADIAN. ) SOLID_ANGLE_UNIT ( ) );
#64159=AXIS2_PLACEMENT_3D ( 'NONE', #17272, #59573, #64804 ) ;
#64303=ORIENTED_EDGE ( 'NONE', *, *, #66051, .T. ) ;
#64343=DIRECTION ( 'NONE',  ( -0.7071067040009368920, 0.000000000000000000, -0.7071068583721498158 ) ) ;
#64415=ORIENTED_EDGE ( 'NONE', *, *, #41401, .F. ) ;
#64442=EDGE_LOOP ( 'NONE', ( #45804, #38162, #37846 ) ) ;
#64571=CIRCLE ( 'NONE', #38940, 2.524999655449999825 ) ;
#64620=ORIENTED_EDGE ( 'NONE', *, *, #13195, .F. ) ;
#64638=EDGE_CURVE ( 'NONE', #57947, #45043, #24198, .T. ) ;
#64667=SHAPE_REPRESENTATION_RELATIONSHIP ( 'NONE' , 'NONE' ,  #19687, #24370 ) ;
#64804=DIRECTION ( 'NONE',  ( 0.000000000000000000, 1.000000000000000000, 0.000000000000000000 ) ) ;
#64812=EDGE_CURVE ( 'NONE', #50185, #4, #68484, .T. ) ;
#65157=DIRECTION ( 'NONE',  ( -1.000000000000000000, 0.000000000000000000, 0.000000000000000000 ) ) ;
#65195=AXIS2_PLACEMENT_3D ( 'NONE', #39300, #65157, #7832 ) ;
#65467=DIRECTION ( 'NONE',  ( 0.000000000000000000, -1.000000000000000000, 0.000000000000000000 ) ) ;
#65476=AXIS2_PLACEMENT_3D ( 'NONE', #13447, #50490, #55745 ) ;
#65486=AXIS2_PLACEMENT_3D ( 'NONE', #15964, #931, #59651 ) ;
#65564=EDGE_CURVE ( 'NONE', #49507, #65786, #12852, .T. ) ;
#65692=ORIENTED_EDGE ( 'NONE', *, *, #16171, .T. ) ;
#65786=VERTEX_POINT ( 'NONE', #54369 ) ;
#65854=EDGE_LOOP ( 'NONE', ( #57437, #175, #9115, #16701 ) ) ;
#65949=CIRCLE ( 'NONE', #54781, 2.725000000000000089 ) ;
#66051=EDGE_CURVE ( 'NONE', #45933, #59889, #39750, .T. ) ;
#66218=CARTESIAN_POINT ( 'NONE',  ( 3.999999855301999752, 0.000000000000000000, -2.524999655449999825 ) ) ;
#66322=EDGE_LOOP ( 'NONE', ( #58997, #788, #27651, #45307 ) ) ;
#66440=CARTESIAN_POINT ( 'NONE',  ( 0.1499996298882999846, -2.250000000000000000, 0.000000000000000000 ) ) ;
#66454=AXIS2_PLACEMENT_3D ( 'NONE', #31245, #52552, #27366 ) ;
#66554=CYLINDRICAL_SURFACE ( 'NONE', #38181, 1.625000000000000000 ) ;
#66641=FACE_OUTER_BOUND ( 'NONE', #63638, .T. ) ;
#66668=ORIENTED_EDGE ( 'NONE', *, *, #35239, .T. ) ;
#66891=ORIENTED_EDGE ( 'NONE', *, *, #18793, .F. ) ;
#66918=CARTESIAN_POINT ( 'NONE',  ( 3.899999503719000060, 0.000000000000000000, 0.000000000000000000 ) ) ;
#67168=DIRECTION ( 'NONE',  ( -0.7071065545305982303, 0.000000000000000000, -0.7071070078424241956 ) ) ;
#67487=ADVANCED_FACE ( 'NONE', ( #11581 ), #38693, .F. ) ;
#67597=DIRECTION ( 'NONE',  ( 0.000000000000000000, 1.000000000000000000, 0.000000000000000000 ) ) ;
#67804=LINE ( 'NONE', #46841, #22383 ) ;
#67940=COLOUR_RGB ( '', 0.40784314, 0.44705882, 0.49803922) ;
#68181=AXIS2_PLACEMENT_3D ( 'NONE', #36316, #20237, #52042 ) ;
#68273=ORIENTED_EDGE ( 'NONE', *, *, #15665, .T. ) ;
#68308=DIRECTION ( 'NONE',  ( 0.000000000000000000, -1.000000000000000000, 0.000000000000000000 ) ) ;
#68484=CIRCLE ( 'NONE', #42853, 2.725000000000000089 ) ;
#68603=ORIENTED_EDGE ( 'NONE', *, *, #7036, .T. ) ;
#68625=DIRECTION ( 'NONE',  ( 1.000000000000000000, 0.000000000000000000, 0.000000000000000000 ) ) ;
#68654=LINE ( 'NONE', #63409, #7949 ) ;
#68894=DIRECTION ( 'NONE',  ( 0.000000000000000000, 1.000000000000000000, 0.000000000000000000 ) ) ;
#68917=AXIS2_PLACEMENT_3D ( 'NONE', #59059, #10468, #37389 ) ;
#68940=CIRCLE ( 'NONE', #10901, 1.775000326287000219 ) ;
#69073=CARTESIAN_POINT ( 'NONE',  ( 1.699999999999999956, 2.250000000000000000, 0.000000000000000000 ) ) ;
#69132=EDGE_CURVE ( 'NONE', #1201, #63599, #59946, .T. ) ;
ENDSEC;
END-ISO-10303-21;
